ISO-10303-21;
HEADER;
/* Generated by software containing ST-Developer
 * from STEP Tools, Inc. (www.steptools.com) 
 */

FILE_DESCRIPTION(
/* description */ ('Air blow-off nozzle station'),
/* implementation_level */ '2;1');

FILE_NAME(
/* name */ 'Ball clamp nut (2).step',
/* time_stamp */ '2026-10-27T10:53:54-07:00',
/* author */ (''),
/* organization */ (''),
/* preprocessor_version */ 'ST-DEVELOPER v20.2',
/* originating_system */ 'Autodesk Translation Framework v15.17.0.0',
/* authorisation */ '');

FILE_SCHEMA (('AUTOMOTIVE_DESIGN { 1 0 10303 214 3 1 1 }'));
ENDSEC;

DATA;
#10=MECHANICAL_DESIGN_GEOMETRIC_PRESENTATION_REPRESENTATION('',(#245),#7897);
#167=SPHERICAL_SURFACE('',#4738,1.);
#195=SHAPE_REPRESENTATION_RELATIONSHIP('SRR','None',#8009,#220);
#220=ADVANCED_BREP_SHAPE_REPRESENTATION('',(#270),#7876);
#245=STYLED_ITEM('',(#8227),#270);
#270=MANIFOLD_SOLID_BREP('Body1',#4294);
#320=FACE_BOUND('',#911,.T.);
#321=FACE_BOUND('',#912,.T.);
#322=FACE_BOUND('',#915,.T.);
#323=FACE_BOUND('',#918,.T.);
#324=FACE_BOUND('',#920,.T.);
#421=PLANE('',#4743);
#422=PLANE('',#4747);
#423=PLANE('',#4748);
#617=FACE_OUTER_BOUND('',#908,.T.);
#618=FACE_OUTER_BOUND('',#909,.T.);
#619=FACE_OUTER_BOUND('',#910,.T.);
#620=FACE_OUTER_BOUND('',#913,.T.);
#621=FACE_OUTER_BOUND('',#914,.T.);
#622=FACE_OUTER_BOUND('',#916,.T.);
#623=FACE_OUTER_BOUND('',#917,.T.);
#624=FACE_OUTER_BOUND('',#919,.T.);
#908=EDGE_LOOP('',(#3227,#3228,#3229,#3230));
#909=EDGE_LOOP('',(#3231,#3232,#3233,#3234));
#910=EDGE_LOOP('',(#3235,#3236));
#911=EDGE_LOOP('',(#3237));
#912=EDGE_LOOP('',(#3238));
#913=EDGE_LOOP('',(#3239,#3240,#3241,#3242));
#914=EDGE_LOOP('',(#3243));
#915=EDGE_LOOP('',(#3244));
#916=EDGE_LOOP('',(#3245,#3246,#3247,#3248));
#917=EDGE_LOOP('',(#3249));
#918=EDGE_LOOP('',(#3250));
#919=EDGE_LOOP('',(#3251));
#920=EDGE_LOOP('',(#3252));
#1232=LINE('',#6992,#1586);
#1233=LINE('',#6998,#1587);
#1234=LINE('',#7008,#1588);
#1235=LINE('',#7015,#1589);
#1586=VECTOR('',#5456,0.4);
#1587=VECTOR('',#5463,0.85);
#1588=VECTOR('',#5474,1.2);
#1589=VECTOR('',#5483,1.4);
#1901=CIRCLE('',#4733,0.4);
#1902=CIRCLE('',#4734,0.4);
#1903=CIRCLE('',#4736,0.85);
#1904=CIRCLE('',#4737,0.85);
#1905=CIRCLE('',#4739,1.);
#1906=CIRCLE('',#4741,1.2);
#1907=CIRCLE('',#4742,1.2);
#1908=CIRCLE('',#4745,1.4);
#1909=CIRCLE('',#4746,1.4);
#2120=VERTEX_POINT('',#6989);
#2121=VERTEX_POINT('',#6991);
#2122=VERTEX_POINT('',#6995);
#2123=VERTEX_POINT('',#6997);
#2124=VERTEX_POINT('',#7001);
#2125=VERTEX_POINT('',#7002);
#2126=VERTEX_POINT('',#7005);
#2127=VERTEX_POINT('',#7007);
#2128=VERTEX_POINT('',#7012);
#2129=VERTEX_POINT('',#7014);
#2531=EDGE_CURVE('',#2120,#2120,#1901,.T.);
#2532=EDGE_CURVE('',#2120,#2121,#1232,.T.);
#2533=EDGE_CURVE('',#2121,#2121,#1902,.T.);
#2534=EDGE_CURVE('',#2122,#2122,#1903,.T.);
#2535=EDGE_CURVE('',#2122,#2123,#1233,.T.);
#2536=EDGE_CURVE('',#2123,#2123,#1904,.T.);
#2537=EDGE_CURVE('',#2124,#2125,#1905,.T.);
#2538=EDGE_CURVE('',#2126,#2126,#1906,.T.);
#2539=EDGE_CURVE('',#2126,#2127,#1234,.T.);
#2540=EDGE_CURVE('',#2127,#2127,#1907,.T.);
#2541=EDGE_CURVE('',#2128,#2128,#1908,.T.);
#2542=EDGE_CURVE('',#2128,#2129,#1235,.T.);
#2543=EDGE_CURVE('',#2129,#2129,#1909,.T.);
#3227=ORIENTED_EDGE('',*,*,#2531,.F.);
#3228=ORIENTED_EDGE('',*,*,#2532,.T.);
#3229=ORIENTED_EDGE('',*,*,#2533,.F.);
#3230=ORIENTED_EDGE('',*,*,#2532,.F.);
#3231=ORIENTED_EDGE('',*,*,#2534,.F.);
#3232=ORIENTED_EDGE('',*,*,#2535,.T.);
#3233=ORIENTED_EDGE('',*,*,#2536,.F.);
#3234=ORIENTED_EDGE('',*,*,#2535,.F.);
#3235=ORIENTED_EDGE('',*,*,#2537,.T.);
#3236=ORIENTED_EDGE('',*,*,#2537,.F.);
#3237=ORIENTED_EDGE('',*,*,#2531,.T.);
#3238=ORIENTED_EDGE('',*,*,#2536,.T.);
#3239=ORIENTED_EDGE('',*,*,#2538,.F.);
#3240=ORIENTED_EDGE('',*,*,#2539,.T.);
#3241=ORIENTED_EDGE('',*,*,#2540,.F.);
#3242=ORIENTED_EDGE('',*,*,#2539,.F.);
#3243=ORIENTED_EDGE('',*,*,#2538,.T.);
#3244=ORIENTED_EDGE('',*,*,#2533,.T.);
#3245=ORIENTED_EDGE('',*,*,#2541,.F.);
#3246=ORIENTED_EDGE('',*,*,#2542,.T.);
#3247=ORIENTED_EDGE('',*,*,#2543,.T.);
#3248=ORIENTED_EDGE('',*,*,#2542,.F.);
#3249=ORIENTED_EDGE('',*,*,#2541,.T.);
#3250=ORIENTED_EDGE('',*,*,#2540,.T.);
#3251=ORIENTED_EDGE('',*,*,#2543,.F.);
#3252=ORIENTED_EDGE('',*,*,#2534,.T.);
#3984=CYLINDRICAL_SURFACE('',#4732,0.4);
#3985=CYLINDRICAL_SURFACE('',#4735,0.85);
#3986=CYLINDRICAL_SURFACE('',#4740,1.2);
#3987=CYLINDRICAL_SURFACE('',#4744,1.4);
#4107=ADVANCED_FACE('',(#617),#3984,.F.);
#4108=ADVANCED_FACE('',(#618),#3985,.F.);
#4109=ADVANCED_FACE('',(#619,#320,#321),#167,.F.);
#4110=ADVANCED_FACE('',(#620),#3986,.T.);
#4111=ADVANCED_FACE('',(#621,#322),#421,.T.);
#4112=ADVANCED_FACE('',(#622),#3987,.T.);
#4113=ADVANCED_FACE('',(#623,#323),#422,.T.);
#4114=ADVANCED_FACE('',(#624,#324),#423,.F.);
#4294=CLOSED_SHELL('',(#4107,#4108,#4109,#4110,#4111,#4112,#4113,#4114));
#4731=AXIS2_PLACEMENT_3D('',#6987,#5450,#5451);
#4732=AXIS2_PLACEMENT_3D('',#6988,#5452,#5453);
#4733=AXIS2_PLACEMENT_3D('',#6990,#5454,#5455);
#4734=AXIS2_PLACEMENT_3D('',#6993,#5457,#5458);
#4735=AXIS2_PLACEMENT_3D('',#6994,#5459,#5460);
#4736=AXIS2_PLACEMENT_3D('',#6996,#5461,#5462);
#4737=AXIS2_PLACEMENT_3D('',#6999,#5464,#5465);
#4738=AXIS2_PLACEMENT_3D('',#7000,#5466,#5467);
#4739=AXIS2_PLACEMENT_3D('',#7003,#5468,#5469);
#4740=AXIS2_PLACEMENT_3D('',#7004,#5470,#5471);
#4741=AXIS2_PLACEMENT_3D('',#7006,#5472,#5473);
#4742=AXIS2_PLACEMENT_3D('',#7009,#5475,#5476);
#4743=AXIS2_PLACEMENT_3D('',#7010,#5477,#5478);
#4744=AXIS2_PLACEMENT_3D('',#7011,#5479,#5480);
#4745=AXIS2_PLACEMENT_3D('',#7013,#5481,#5482);
#4746=AXIS2_PLACEMENT_3D('',#7016,#5484,#5485);
#4747=AXIS2_PLACEMENT_3D('',#7017,#5486,#5487);
#4748=AXIS2_PLACEMENT_3D('',#7018,#5488,#5489);
#5450=DIRECTION('axis',(0.,0.,1.));
#5451=DIRECTION('refdir',(1.,0.,0.));
#5452=DIRECTION('center_axis',(0.,1.,0.));
#5453=DIRECTION('ref_axis',(1.,0.,0.));
#5454=DIRECTION('center_axis',(0.,1.,0.));
#5455=DIRECTION('ref_axis',(1.,0.,0.));
#5456=DIRECTION('',(0.,1.,0.));
#5457=DIRECTION('center_axis',(0.,-1.,0.));
#5458=DIRECTION('ref_axis',(1.,0.,0.));
#5459=DIRECTION('center_axis',(0.,1.,0.));
#5460=DIRECTION('ref_axis',(1.,0.,0.));
#5461=DIRECTION('center_axis',(0.,1.,0.));
#5462=DIRECTION('ref_axis',(1.,0.,0.));
#5463=DIRECTION('',(0.,1.,0.));
#5464=DIRECTION('center_axis',(0.,-1.,0.));
#5465=DIRECTION('ref_axis',(1.,0.,0.));
#5466=DIRECTION('center_axis',(0.,0.,1.));
#5467=DIRECTION('ref_axis',(1.,0.,0.));
#5468=DIRECTION('center_axis',(0.,1.,0.));
#5469=DIRECTION('ref_axis',(-1.,0.,0.));
#5470=DIRECTION('center_axis',(0.,1.,0.));
#5471=DIRECTION('ref_axis',(1.,0.,0.));
#5472=DIRECTION('center_axis',(0.,1.,0.));
#5473=DIRECTION('ref_axis',(1.,0.,0.));
#5474=DIRECTION('',(0.,-1.,0.));
#5475=DIRECTION('center_axis',(0.,-1.,0.));
#5476=DIRECTION('ref_axis',(1.,0.,0.));
#5477=DIRECTION('center_axis',(0.,1.,0.));
#5478=DIRECTION('ref_axis',(1.,0.,0.));
#5479=DIRECTION('center_axis',(0.,1.,0.));
#5480=DIRECTION('ref_axis',(1.,0.,0.));
#5481=DIRECTION('center_axis',(0.,1.,0.));
#5482=DIRECTION('ref_axis',(1.,0.,0.));
#5483=DIRECTION('',(0.,-1.,0.));
#5484=DIRECTION('center_axis',(0.,1.,0.));
#5485=DIRECTION('ref_axis',(1.,0.,0.));
#5486=DIRECTION('center_axis',(0.,1.,0.));
#5487=DIRECTION('ref_axis',(1.,0.,0.));
#5488=DIRECTION('center_axis',(0.,1.,0.));
#5489=DIRECTION('ref_axis',(1.,0.,0.));
#6987=CARTESIAN_POINT('',(0.,0.,0.));
#6988=CARTESIAN_POINT('Origin',(3.,-2.1,23.));
#6989=CARTESIAN_POINT('',(2.6,-1.08348486100883,23.));
#6990=CARTESIAN_POINT('Origin',(3.,-1.08348486100883,23.));
#6991=CARTESIAN_POINT('',(2.6,-1.,23.));
#6992=CARTESIAN_POINT('',(2.6,-2.1,23.));
#6993=CARTESIAN_POINT('Origin',(3.,-1.,23.));
#6994=CARTESIAN_POINT('Origin',(3.,-3.3,23.));
#6995=CARTESIAN_POINT('',(2.15,-3.2,23.));
#6996=CARTESIAN_POINT('Origin',(3.,-3.2,23.));
#6997=CARTESIAN_POINT('',(2.15,-2.52678268764264,23.));
#6998=CARTESIAN_POINT('',(2.15,-3.3,23.));
#6999=CARTESIAN_POINT('Origin',(3.,-2.52678268764264,23.));
#7000=CARTESIAN_POINT('Origin',(3.,-2.,23.));
#7001=CARTESIAN_POINT('',(3.,-2.,22.));
#7002=CARTESIAN_POINT('',(3.,-2.,24.));
#7003=CARTESIAN_POINT('Origin',(3.,-2.,23.));
#7004=CARTESIAN_POINT('Origin',(3.,-1.5,23.));
#7005=CARTESIAN_POINT('',(1.8,-1.,23.));
#7006=CARTESIAN_POINT('Origin',(3.,-1.,23.));
#7007=CARTESIAN_POINT('',(1.8,-1.5,23.));
#7008=CARTESIAN_POINT('',(1.8,-1.5,23.));
#7009=CARTESIAN_POINT('Origin',(3.,-1.5,23.));
#7010=CARTESIAN_POINT('Origin',(3.,-1.,23.));
#7011=CARTESIAN_POINT('Origin',(3.,-3.2,23.));
#7012=CARTESIAN_POINT('',(1.6,-1.5,23.));
#7013=CARTESIAN_POINT('Origin',(3.,-1.5,23.));
#7014=CARTESIAN_POINT('',(1.6,-3.2,23.));
#7015=CARTESIAN_POINT('',(1.6,-3.2,23.));
#7016=CARTESIAN_POINT('Origin',(3.,-3.2,23.));
#7017=CARTESIAN_POINT('Origin',(3.,-1.5,23.));
#7018=CARTESIAN_POINT('Origin',(3.,-3.2,23.));
#7844=UNCERTAINTY_MEASURE_WITH_UNIT(LENGTH_MEASURE(0.001),#7898,
'DISTANCE_ACCURACY_VALUE',
'Maximum model space distance between geometric entities at asserted c
onnectivities');
#7865=UNCERTAINTY_MEASURE_WITH_UNIT(LENGTH_MEASURE(0.001),#7898,
'DISTANCE_ACCURACY_VALUE',
'Maximum model space distance between geometric entities at asserted c
onnectivities');
#7876=(
GEOMETRIC_REPRESENTATION_CONTEXT(3)
GLOBAL_UNCERTAINTY_ASSIGNED_CONTEXT((#7844))
GLOBAL_UNIT_ASSIGNED_CONTEXT((#7898,#7900,#7901))
REPRESENTATION_CONTEXT('','3D')
);
#7897=(
GEOMETRIC_REPRESENTATION_CONTEXT(3)
GLOBAL_UNCERTAINTY_ASSIGNED_CONTEXT((#7865))
GLOBAL_UNIT_ASSIGNED_CONTEXT((#7898,#7900,#7901))
REPRESENTATION_CONTEXT('','3D')
);
#7898=(
LENGTH_UNIT()
NAMED_UNIT(*)
SI_UNIT(.CENTI.,.METRE.)
);
#7900=(
NAMED_UNIT(*)
PLANE_ANGLE_UNIT()
SI_UNIT($,.RADIAN.)
);
#7901=(
NAMED_UNIT(*)
SI_UNIT($,.STERADIAN.)
SOLID_ANGLE_UNIT()
);
#7912=SHAPE_DEFINITION_REPRESENTATION(#7943,#8009);
#7943=PRODUCT_DEFINITION_SHAPE('',$,#8041);
#8009=SHAPE_REPRESENTATION('',(#4731),#7876);
#8030=PRODUCT_DEFINITION_CONTEXT('part definition',#8125,'design');
#8041=PRODUCT_DEFINITION('Ball clamp nut (2)','Ball clamp nut (2)',#8072,
#8030);
#8072=PRODUCT_DEFINITION_FORMATION('',$,#8137);
#8125=APPLICATION_CONTEXT(
'Core Data for Automotive Mechanical Design Process');
#8126=PRODUCT_CONTEXT('part definition',#8125,'mechanical');
#8137=PRODUCT('Ball clamp nut (2)','Ball clamp nut (2)','Ball clamp nut (2)',
(#8126));
#8221=COLOUR_RGB('Black',0.12,0.14,0.17);
#8222=FILL_AREA_STYLE_COLOUR('',#8221);
#8223=FILL_AREA_STYLE('',(#8222));
#8224=SURFACE_STYLE_FILL_AREA(#8223);
#8225=SURFACE_SIDE_STYLE('',(#8224));
#8226=SURFACE_STYLE_USAGE(.BOTH.,#8225);
#8227=PRESENTATION_STYLE_ASSIGNMENT((#8226));
ENDSEC;
END-ISO-10303-21;
